ISO-10303-21;
HEADER;
FILE_DESCRIPTION (('STEP AP214'),
    '1' );
FILE_NAME ('O Ring Seal 1.step',
    '2026-10-05T22:38:29',
    ( '' ),
    ( '' ),
    'SwSTEP 2.0',
    'SolidWorks 2020',
    '' );
FILE_SCHEMA (( 'AUTOMOTIVE_DESIGN' ));
ENDSEC;

DATA;
#262=AXIS2_PLACEMENT_3D ( 'NONE', #53883, #16817, #11569 ) ;
#312=PRODUCT_DEFINITION_CONTEXT ( 'detailed design', #15925, 'design' ) ;
#1054=SURFACE_STYLE_FILL_AREA ( #22016 ) ;
#1430=CIRCLE ( 'NONE', #49428, 11.84999999999999964 ) ;
#1591=DIRECTION ( 'NONE',  ( 1.000000000000000000, 0.000000000000000000, 0.000000000000000000 ) ) ;
#1666=PRODUCT_DEFINITION_FORMATION_WITH_SPECIFIED_SOURCE ( 'ANY', '', #8728, .NOT_KNOWN. ) ;
#2301=ADVANCED_FACE ( 'NONE', ( #64843 ), #49383, .T. ) ;
#2321=CIRCLE ( 'NONE', #7914, 11.84999999999999964 ) ;
#2514=( NAMED_UNIT ( * ) SI_UNIT ( $, .STERADIAN. ) SOLID_ANGLE_UNIT ( ) );
#2516=DIRECTION ( 'NONE',  ( 1.000000000000000000, 0.000000000000000000, 0.000000000000000000 ) ) ;
#3189=ORIENTED_EDGE ( 'NONE', *, *, #34206, .T. ) ;
#3225=DIRECTION ( 'NONE',  ( -2.154007395656495261E-21, 3.276905819395100166E-06, -0.9999999999946310725 ) ) ;
#4105=DIRECTION ( 'NONE',  ( 0.000000000000000000, 1.000000000000000000, 0.000000000000000000 ) ) ;
#4450=DIRECTION ( 'NONE',  ( -1.000000000000000000, 0.000000000000000000, 0.000000000000000000 ) ) ;
#4742=DIRECTION ( 'NONE',  ( 0.000000000000000000, -0.9999808993455937545, -0.006180691221632959691 ) ) ;
#4852=FACE_OUTER_BOUND ( 'NONE', #20720, .T. ) ;
#5186=DIRECTION ( 'NONE',  ( 0.000000000000000000, -1.000000000000000000, 0.000000000000000000 ) ) ;
#6023=FACE_OUTER_BOUND ( 'NONE', #21736, .T. ) ;
#6481=CARTESIAN_POINT ( 'NONE',  ( 9.099999999999999645, 11.84999999999999964, 0.000000000000000000 ) ) ;
#6706=CARTESIAN_POINT ( 'NONE',  ( 9.099999999999999645, 0.000000000000000000, 0.000000000000000000 ) ) ;
#6744=CARTESIAN_POINT ( 'NONE',  ( 10.10000000000000142, 0.000000000000000000, 0.000000000000000000 ) ) ;
#7037=MANIFOLD_SOLID_BREP ( 'Stock-MAS-678-1', #49290 ) ;
#7058=DIRECTION ( 'NONE',  ( 0.000000000000000000, 1.000000000000000000, 0.000000000000000000 ) ) ;
#7108=UNCERTAINTY_MEASURE_WITH_UNIT (LENGTH_MEASURE( 1.000000000000000082E-05 ), #28402, 'distance_accuracy_value', 'NONE');
#7169=CIRCLE ( 'NONE', #23943, 11.84999999999999964 ) ;
#7409=SHAPE_REPRESENTATION_RELATIONSHIP ( 'NONE' , 'NONE' ,  #22871, #30277 ) ;
#7914=AXIS2_PLACEMENT_3D ( 'NONE', #63210, #53086, #5186 ) ;
#8110=PRESENTATION_STYLE_ASSIGNMENT (( #29453 ) ) ;
#8187=DIRECTION ( 'NONE',  ( -1.000000000000000000, 0.000000000000000000, 0.000000000000000000 ) ) ;
#8229=VERTEX_POINT ( 'NONE', #20308 ) ;
#8283=ORIENTED_EDGE ( 'NONE', *, *, #21319, .T. ) ;
#8728=PRODUCT ( 'O Ring Seal 1', 'O Ring Seal 1', '', ( #51573 ) ) ;
#9393=ADVANCED_FACE ( 'NONE', ( #59157, #33640 ), #11261, .F. ) ;
#9676=AXIS2_PLACEMENT_3D ( 'NONE', #40345, #19020, #18341 ) ;
#10800=UNCERTAINTY_MEASURE_WITH_UNIT (LENGTH_MEASURE( 1.000000000000000082E-05 ), #56258, 'distance_accuracy_value', 'NONE');
#11261=PLANE ( 'NONE',  #52243 ) ;
#11569=DIRECTION ( 'NONE',  ( 0.000000000000000000, 1.000000000000000000, 0.000000000000000000 ) ) ;
#11715=ORIENTED_EDGE ( 'NONE', *, *, #35158, .F. ) ;
#11984=DIRECTION ( 'NONE',  ( 0.000000000000000000, -1.000000000000000000, 0.000000000000000000 ) ) ;
#11996=FACE_OUTER_BOUND ( 'NONE', #63726, .T. ) ;
#12465=ORIENTED_EDGE ( 'NONE', *, *, #60785, .F. ) ;
#14049=CARTESIAN_POINT ( 'NONE',  ( 9.099999999999999645, -11.84999999999999964, 0.000000000000000000 ) ) ;
#14099=EDGE_CURVE ( 'NONE', #8229, #24046, #68892, .T. ) ;
#15041=DIRECTION ( 'NONE',  ( -1.000000000000000000, 0.000000000000000000, 0.000000000000000000 ) ) ;
#15872=CIRCLE ( 'NONE', #262, 12.35000000006999876 ) ;
#15925=APPLICATION_CONTEXT ( 'automotive_design' ) ;
#15968=ORIENTED_EDGE ( 'NONE', *, *, #29144, .F. ) ;
#16371=AXIS2_PLACEMENT_3D ( 'NONE', #40014, #8187, #61328 ) ;
#16817=DIRECTION ( 'NONE',  ( -1.000000000000000000, 0.000000000000000000, 0.000000000000000000 ) ) ;
#16977=DIRECTION ( 'NONE',  ( 0.000000000000000000, -1.000000000000000000, 0.000000000000000000 ) ) ;
#16984=CIRCLE ( 'NONE', #56076, 0.4999999999999997224 ) ;
#17212=DIRECTION ( 'NONE',  ( 1.000000000000000000, 0.000000000000000000, 0.000000000000000000 ) ) ;
#17448=ORIENTED_EDGE ( 'NONE', *, *, #34206, .F. ) ;
#17512=CARTESIAN_POINT ( 'NONE',  ( 10.10000000000000142, -11.84999999999999964, 0.000000000000000000 ) ) ;
#17831=VERTEX_POINT ( 'NONE', #41283 ) ;
#18341=DIRECTION ( 'NONE',  ( 1.000000000000000000, 0.000000000000000000, 0.000000000000000000 ) ) ;
#18472=CARTESIAN_POINT ( 'NONE',  ( 10.10000000000000142, -12.35000000006999876, 0.000000000000000000 ) ) ;
#18593=AXIS2_PLACEMENT_3D ( 'NONE', #67735, #4450, #57249 ) ;
#18907=EDGE_LOOP ( 'NONE', ( #41848, #11715, #17448, #51647 ) ) ;
#19020=DIRECTION ( 'NONE',  ( 0.000000000000000000, 0.000000000000000000, 1.000000000000000000 ) ) ;
#20194=DIRECTION ( 'NONE',  ( -1.000000000000000000, 0.000000000000000000, 0.000000000000000000 ) ) ;
#20235=TOROIDAL_SURFACE ( 'NONE', #28075, 12.35000000006999876, 0.5000000000000000000 ) ;
#20308=CARTESIAN_POINT ( 'NONE',  ( 10.10000000000000142, 12.35000000006999876, 0.000000000000000000 ) ) ;
#20353=VERTEX_POINT ( 'NONE', #35812 ) ;
#20720=EDGE_LOOP ( 'NONE', ( #63051, #15968, #40458, #8283 ) ) ;
#21319=EDGE_CURVE ( 'NONE', #17831, #40269, #2321, .T. ) ;
#21429=AXIS2_PLACEMENT_3D ( 'NONE', #26783, #38287, #4742 ) ;
#21509=ORIENTED_EDGE ( 'NONE', *, *, #26268, .F. ) ;
#21733=CARTESIAN_POINT ( 'NONE',  ( 9.600000000000001421, 12.34999999999999964, 4.046978687741000012E-05 ) ) ;
#21736=EDGE_LOOP ( 'NONE', ( #3189, #24736, #53364, #45254 ) ) ;
#21857=( GEOMETRIC_REPRESENTATION_CONTEXT ( 3 ) GLOBAL_UNCERTAINTY_ASSIGNED_CONTEXT ( ( #10800 ) ) GLOBAL_UNIT_ASSIGNED_CONTEXT ( ( #56258, #56600, #23752 ) ) REPRESENTATION_CONTEXT ( 'NONE', 'WORKASPACE' ) );
#22016=FILL_AREA_STYLE ('',( #32522 ) ) ;
#22871=SHAPE_REPRESENTATION ( 'O Ring Seal 1', ( #9676 ), #49917 ) ;
#22961=COLOUR_RGB ( '', 0.31764706, 0.68627451, 0.89019608) ;
#23166=CYLINDRICAL_SURFACE ( 'NONE', #63269, 11.84999999999999964 ) ;
#23208=ADVANCED_FACE ( 'NONE', ( #6023 ), #20235, .T. ) ;
#23522=DIRECTION ( 'NONE',  ( 1.000000000000000000, 0.000000000000000000, 0.000000000000000000 ) ) ;
#23752=( NAMED_UNIT ( * ) SI_UNIT ( $, .STERADIAN. ) SOLID_ANGLE_UNIT ( ) );
#23943=AXIS2_PLACEMENT_3D ( 'NONE', #36625, #20194, #4105 ) ;
#24046=VERTEX_POINT ( 'NONE', #40692 ) ;
#24177=CARTESIAN_POINT ( 'NONE',  ( 9.099999999999999645, 11.84999999999999964, 0.000000000000000000 ) ) ;
#24269=MECHANICAL_DESIGN_GEOMETRIC_PRESENTATION_REPRESENTATION('',(#35457),#33206);
#24736=ORIENTED_EDGE ( 'NONE', *, *, #67774, .F. ) ;
#24746=ADVANCED_FACE ( 'NONE', ( #65462 ), #23166, .F. ) ;
#25027=ORIENTED_EDGE ( 'NONE', *, *, #67774, .T. ) ;
#25232=DIRECTION ( 'NONE',  ( 0.9999999999938153916, 3.516990153967782703E-06, 1.152484550329262306E-11 ) ) ;
#26268=EDGE_CURVE ( 'NONE', #42155, #8229, #29831, .T. ) ;
#26783=CARTESIAN_POINT ( 'NONE',  ( 9.600000000000001421, 0.000000000000000000, 0.000000000000000000 ) ) ;
#28060=CARTESIAN_POINT ( 'NONE',  ( 9.099999999999999645, 0.000000000000000000, 0.000000000000000000 ) ) ;
#28075=AXIS2_PLACEMENT_3D ( 'NONE', #54266, #17212, #59170 ) ;
#28084=DIRECTION ( 'NONE',  ( 0.000000000000000000, 1.000000000000000000, 0.000000000000000000 ) ) ;
#28229=ORIENTED_EDGE ( 'NONE', *, *, #60785, .T. ) ;
#28402=( LENGTH_UNIT ( ) NAMED_UNIT ( * ) SI_UNIT ( .MILLI., .METRE. ) );
#28406=DIRECTION ( 'NONE',  ( -1.000000000000000000, 0.000000000000000000, 0.000000000000000000 ) ) ;
#29105=( NAMED_UNIT ( * ) SI_UNIT ( $, .STERADIAN. ) SOLID_ANGLE_UNIT ( ) );
#29144=EDGE_CURVE ( 'NONE', #67057, #20353, #1430, .T. ) ;
#29309=ORIENTED_EDGE ( 'NONE', *, *, #57860, .T. ) ;
#29453=SURFACE_STYLE_USAGE ( .BOTH. , #44145 ) ;
#29831=CIRCLE ( 'NONE', #16371, 12.35000000006999876 ) ;
#29929=VECTOR ( 'NONE', #1591, 1000.000000000000000 ) ;
#30277=ADVANCED_BREP_SHAPE_REPRESENTATION ( '', ( #7037, #9676 ), #49917 ) ;
#31908=MECHANICAL_DESIGN_GEOMETRIC_PRESENTATION_REPRESENTATION('',(#32994),#21857);
#32256=VERTEX_POINT ( 'NONE', #58464 ) ;
#32522=FILL_AREA_STYLE_COLOUR ( '', #22961 ) ;
#32885=APPLICATION_CONTEXT ( 'automotive_design' ) ;
#32927=DIRECTION ( 'NONE',  ( 0.9999999999938153916, -3.516990153967782703E-06, -1.152484550329262306E-11 ) ) ;
#32994=STYLED_ITEM ( 'NONE', ( #55575 ), #7037 ) ;
#33122=ORIENTED_EDGE ( 'NONE', *, *, #51165, .F. ) ;
#33206=( GEOMETRIC_REPRESENTATION_CONTEXT ( 3 ) GLOBAL_UNCERTAINTY_ASSIGNED_CONTEXT ( ( #7108 ) ) GLOBAL_UNIT_ASSIGNED_CONTEXT ( ( #28402, #34345, #2514 ) ) REPRESENTATION_CONTEXT ( 'NONE', 'WORKASPACE' ) );
#33640=FACE_OUTER_BOUND ( 'NONE', #66149, .T. ) ;
#33994=( LENGTH_UNIT ( ) NAMED_UNIT ( * ) SI_UNIT ( .MILLI., .METRE. ) );
#34206=EDGE_CURVE ( 'NONE', #42155, #32256, #16984, .T. ) ;
#34345=( NAMED_UNIT ( * ) PLANE_ANGLE_UNIT ( ) SI_UNIT ( $, .RADIAN. ) );
#35158=EDGE_CURVE ( 'NONE', #32256, #24046, #62878, .T. ) ;
#35457=STYLED_ITEM ( 'NONE', ( #8110 ), #30277 ) ;
#35675=EDGE_CURVE ( 'NONE', #17831, #67057, #55314, .T. ) ;
#35812=CARTESIAN_POINT ( 'NONE',  ( 10.10000000000000142, 11.84999999999999964, 0.000000000000000000 ) ) ;
#35843=SHAPE_DEFINITION_REPRESENTATION ( #62322, #22871 ) ;
#36144=VECTOR ( 'NONE', #2516, 1000.000000000000000 ) ;
#36311=AXIS2_PLACEMENT_3D ( 'NONE', #28060, #28406, #49370 ) ;
#36625=CARTESIAN_POINT ( 'NONE',  ( 10.10000000000000142, 0.000000000000000000, 0.000000000000000000 ) ) ;
#36721=DIRECTION ( 'NONE',  ( 0.000000000000000000, -1.000000000000000000, 0.000000000000000000 ) ) ;
#37669=ADVANCED_FACE ( 'NONE', ( #59887, #11996 ), #54650, .T. ) ;
#38196=ADVANCED_FACE ( 'NONE', ( #4852 ), #43917, .F. ) ;
#38207=DIRECTION ( 'NONE',  ( 1.000000000000000000, 0.000000000000000000, 0.000000000000000000 ) ) ;
#38287=DIRECTION ( 'NONE',  ( 1.000000000000000000, 0.000000000000000000, 0.000000000000000000 ) ) ;
#38557=CARTESIAN_POINT ( 'NONE',  ( 9.600000000000001421, -12.34999999999999964, -4.046978686977000011E-05 ) ) ;
#39014=DIRECTION ( 'NONE',  ( -1.000000000000000000, 0.000000000000000000, 0.000000000000000000 ) ) ;
#39480=ORIENTED_EDGE ( 'NONE', *, *, #35675, .T. ) ;
#40014=CARTESIAN_POINT ( 'NONE',  ( 10.10000000000000142, 0.000000000000000000, 0.000000000000000000 ) ) ;
#40269=VERTEX_POINT ( 'NONE', #24177 ) ;
#40345=CARTESIAN_POINT ( 'NONE',  ( 0.000000000000000000, 0.000000000000000000, 0.000000000000000000 ) ) ;
#40439=EDGE_CURVE ( 'NONE', #8229, #42155, #15872, .T. ) ;
#40458=ORIENTED_EDGE ( 'NONE', *, *, #35675, .F. ) ;
#40692=CARTESIAN_POINT ( 'NONE',  ( 9.099999999999999645, 12.35000000006999876, 0.000000000000000000 ) ) ;
#41165=ORIENTED_EDGE ( 'NONE', *, *, #21319, .F. ) ;
#41283=CARTESIAN_POINT ( 'NONE',  ( 9.099999999999999645, -11.84999999999999964, 0.000000000000000000 ) ) ;
#41848=ORIENTED_EDGE ( 'NONE', *, *, #14099, .T. ) ;
#42155=VERTEX_POINT ( 'NONE', #18472 ) ;
#42281=DIRECTION ( 'NONE',  ( 1.000000000000000000, 0.000000000000000000, 0.000000000000000000 ) ) ;
#43066=DIRECTION ( 'NONE',  ( -4.331025598861020273E-21, -3.276905820014099985E-06, 0.9999999999946310725 ) ) ;
#43657=ORIENTED_EDGE ( 'NONE', *, *, #40439, .F. ) ;
#43917=CYLINDRICAL_SURFACE ( 'NONE', #54104, 11.84999999999999964 ) ;
#44145=SURFACE_SIDE_STYLE ('',( #44833 ) ) ;
#44396=EDGE_LOOP ( 'NONE', ( #29309, #62198 ) ) ;
#44833=SURFACE_STYLE_FILL_AREA ( #51102 ) ;
#45254=ORIENTED_EDGE ( 'NONE', *, *, #40439, .T. ) ;
#47181=UNCERTAINTY_MEASURE_WITH_UNIT (LENGTH_MEASURE( 1.000000000000000082E-05 ), #33994, 'distance_accuracy_value', 'NONE');
#49290=CLOSED_SHELL ( 'NONE', ( #2301, #23208, #37669, #24746, #38196, #9393 ) ) ;
#49370=DIRECTION ( 'NONE',  ( 0.000000000000000000, 1.000000000000000000, 0.000000000000000000 ) ) ;
#49383=TOROIDAL_SURFACE ( 'NONE', #21429, 12.35000000006999876, 0.5000000000000000000 ) ;
#49428=AXIS2_PLACEMENT_3D ( 'NONE', #62583, #15041, #36721 ) ;
#49917=( GEOMETRIC_REPRESENTATION_CONTEXT ( 3 ) GLOBAL_UNCERTAINTY_ASSIGNED_CONTEXT ( ( #47181 ) ) GLOBAL_UNIT_ASSIGNED_CONTEXT ( ( #33994, #50762, #29105 ) ) REPRESENTATION_CONTEXT ( 'NONE', 'WORKASPACE' ) );
#50762=( NAMED_UNIT ( * ) PLANE_ANGLE_UNIT ( ) SI_UNIT ( $, .RADIAN. ) );
#51012=SURFACE_STYLE_USAGE ( .BOTH. , #53838 ) ;
#51102=FILL_AREA_STYLE ('',( #60902 ) ) ;
#51165=EDGE_CURVE ( 'NONE', #40269, #20353, #65556, .T. ) ;
#51573=PRODUCT_CONTEXT ( 'NONE', #32885, 'mechanical' ) ;
#51647=ORIENTED_EDGE ( 'NONE', *, *, #26268, .T. ) ;
#51754=PRODUCT_DEFINITION ( 'UNKNOWN', '', #1666, #312 ) ;
#51810=AXIS2_PLACEMENT_3D ( 'NONE', #6744, #23522, #28084 ) ;
#52243=AXIS2_PLACEMENT_3D ( 'NONE', #6706, #54956, #7058 ) ;
#52759=CARTESIAN_POINT ( 'NONE',  ( 9.099999999999999645, 0.000000000000000000, 0.000000000000000000 ) ) ;
#52862=AXIS2_PLACEMENT_3D ( 'NONE', #64864, #39014, #16977 ) ;
#53086=DIRECTION ( 'NONE',  ( -1.000000000000000000, 0.000000000000000000, 0.000000000000000000 ) ) ;
#53364=ORIENTED_EDGE ( 'NONE', *, *, #14099, .F. ) ;
#53838=SURFACE_SIDE_STYLE ('',( #1054 ) ) ;
#53883=CARTESIAN_POINT ( 'NONE',  ( 10.10000000000000142, 0.000000000000000000, 0.000000000000000000 ) ) ;
#53917=EDGE_LOOP ( 'NONE', ( #39480, #58660, #33122, #28229 ) ) ;
#54104=AXIS2_PLACEMENT_3D ( 'NONE', #52759, #42281, #58687 ) ;
#54266=CARTESIAN_POINT ( 'NONE',  ( 9.600000000000001421, 0.000000000000000000, 0.000000000000000000 ) ) ;
#54650=PLANE ( 'NONE',  #51810 ) ;
#54956=DIRECTION ( 'NONE',  ( 1.000000000000000000, 0.000000000000000000, 0.000000000000000000 ) ) ;
#55314=LINE ( 'NONE', #14049, #36144 ) ;
#55416=CIRCLE ( 'NONE', #18593, 12.35000000006999876 ) ;
#55575=PRESENTATION_STYLE_ASSIGNMENT (( #51012 ) ) ;
#56076=AXIS2_PLACEMENT_3D ( 'NONE', #38557, #3225, #25232 ) ;
#56258=( LENGTH_UNIT ( ) NAMED_UNIT ( * ) SI_UNIT ( .MILLI., .METRE. ) );
#56600=( NAMED_UNIT ( * ) PLANE_ANGLE_UNIT ( ) SI_UNIT ( $, .RADIAN. ) );
#56932=ORIENTED_EDGE ( 'NONE', *, *, #35158, .T. ) ;
#57249=DIRECTION ( 'NONE',  ( 0.000000000000000000, 1.000000000000000000, 0.000000000000000000 ) ) ;
#57860=EDGE_CURVE ( 'NONE', #20353, #67057, #7169, .T. ) ;
#58464=CARTESIAN_POINT ( 'NONE',  ( 9.099999999999999645, -12.35000000006999876, 0.000000000000000000 ) ) ;
#58660=ORIENTED_EDGE ( 'NONE', *, *, #57860, .F. ) ;
#58687=DIRECTION ( 'NONE',  ( 0.000000000000000000, -1.000000000000000000, 0.000000000000000000 ) ) ;
#59157=FACE_BOUND ( 'NONE', #62972, .T. ) ;
#59170=DIRECTION ( 'NONE',  ( 0.000000000000000000, 0.9999808993455937545, 0.006180691221632959691 ) ) ;
#59764=CIRCLE ( 'NONE', #36311, 11.84999999999999964 ) ;
#59878=CARTESIAN_POINT ( 'NONE',  ( 9.099999999999999645, 0.000000000000000000, 0.000000000000000000 ) ) ;
#59887=FACE_BOUND ( 'NONE', #44396, .T. ) ;
#59992=COLOUR_RGB ( '', 0.31764706, 0.68627451, 0.89019608) ;
#60785=EDGE_CURVE ( 'NONE', #40269, #17831, #59764, .T. ) ;
#60902=FILL_AREA_STYLE_COLOUR ( '', #59992 ) ;
#61075=AXIS2_PLACEMENT_3D ( 'NONE', #21733, #43066, #32927 ) ;
#61328=DIRECTION ( 'NONE',  ( 0.000000000000000000, -1.000000000000000000, 0.000000000000000000 ) ) ;
#62198=ORIENTED_EDGE ( 'NONE', *, *, #29144, .T. ) ;
#62322=PRODUCT_DEFINITION_SHAPE ( 'NONE', 'NONE',  #51754 ) ;
#62583=CARTESIAN_POINT ( 'NONE',  ( 10.10000000000000142, 0.000000000000000000, 0.000000000000000000 ) ) ;
#62878=CIRCLE ( 'NONE', #52862, 12.35000000006999876 ) ;
#62972=EDGE_LOOP ( 'NONE', ( #12465, #41165 ) ) ;
#63051=ORIENTED_EDGE ( 'NONE', *, *, #51165, .T. ) ;
#63210=CARTESIAN_POINT ( 'NONE',  ( 9.099999999999999645, 0.000000000000000000, 0.000000000000000000 ) ) ;
#63269=AXIS2_PLACEMENT_3D ( 'NONE', #59878, #38207, #11984 ) ;
#63726=EDGE_LOOP ( 'NONE', ( #21509, #43657 ) ) ;
#64843=FACE_OUTER_BOUND ( 'NONE', #18907, .T. ) ;
#64864=CARTESIAN_POINT ( 'NONE',  ( 9.099999999999999645, 0.000000000000000000, 0.000000000000000000 ) ) ;
#65462=FACE_OUTER_BOUND ( 'NONE', #53917, .T. ) ;
#65556=LINE ( 'NONE', #6481, #29929 ) ;
#66149=EDGE_LOOP ( 'NONE', ( #56932, #25027 ) ) ;
#67057=VERTEX_POINT ( 'NONE', #17512 ) ;
#67735=CARTESIAN_POINT ( 'NONE',  ( 9.099999999999999645, 0.000000000000000000, 0.000000000000000000 ) ) ;
#67774=EDGE_CURVE ( 'NONE', #24046, #32256, #55416, .T. ) ;
#68892=CIRCLE ( 'NONE', #61075, 0.4999999999999997224 ) ;
ENDSEC;
END-ISO-10303-21;
